ISO-10303-21;
HEADER;
/* Generated by software containing ST-Developer
 * from STEP Tools, Inc. (www.steptools.com) 
 */

FILE_DESCRIPTION(
/* description */ ('Flywheel Crank-Slider'),
/* implementation_level */ '2;1');

FILE_NAME(
/* name */ 'Pin keeper (1).step',
/* time_stamp */ '2026-10-28T03:23:13-07:00',
/* author */ (''),
/* organization */ (''),
/* preprocessor_version */ 'ST-DEVELOPER v20.2',
/* originating_system */ 'Autodesk Translation Framework v15.17.0.0',
/* authorisation */ '');

FILE_SCHEMA (('AUTOMOTIVE_DESIGN { 1 0 10303 214 3 1 1 }'));
ENDSEC;

DATA;
#10=MECHANICAL_DESIGN_GEOMETRIC_PRESENTATION_REPRESENTATION('',(#725),#17322);
#612=SHAPE_REPRESENTATION_RELATIONSHIP('SRR','None',#17613,#664);
#664=ADVANCED_BREP_SHAPE_REPRESENTATION('',(#782),#17317);
#725=STYLED_ITEM('',(#17931),#782);
#782=MANIFOLD_SOLID_BREP('Body1',#9107);
#997=FACE_BOUND('',#2560,.T.);
#998=FACE_BOUND('',#2562,.T.);
#1290=PLANE('',#10657);
#1291=PLANE('',#10658);
#1810=FACE_OUTER_BOUND('',#2557,.T.);
#1811=FACE_OUTER_BOUND('',#2558,.T.);
#1812=FACE_OUTER_BOUND('',#2559,.T.);
#1813=FACE_OUTER_BOUND('',#2561,.T.);
#2557=EDGE_LOOP('',(#8162,#8163,#8164,#8165));
#2558=EDGE_LOOP('',(#8166,#8167,#8168,#8169));
#2559=EDGE_LOOP('',(#8170));
#2560=EDGE_LOOP('',(#8171));
#2561=EDGE_LOOP('',(#8172));
#2562=EDGE_LOOP('',(#8173));
#3176=LINE('',#16920,#3787);
#3177=LINE('',#16926,#3788);
#3787=VECTOR('',#13326,0.225);
#3788=VECTOR('',#13333,0.800000000000001);
#4244=CIRCLE('',#10652,0.225);
#4245=CIRCLE('',#10653,0.225);
#4246=CIRCLE('',#10655,0.800000000000001);
#4247=CIRCLE('',#10656,0.800000000000001);
#4963=VERTEX_POINT('',#16917);
#4964=VERTEX_POINT('',#16919);
#4965=VERTEX_POINT('',#16923);
#4966=VERTEX_POINT('',#16925);
#6038=EDGE_CURVE('',#4963,#4963,#4244,.T.);
#6039=EDGE_CURVE('',#4963,#4964,#3176,.T.);
#6040=EDGE_CURVE('',#4964,#4964,#4245,.T.);
#6041=EDGE_CURVE('',#4965,#4965,#4246,.T.);
#6042=EDGE_CURVE('',#4965,#4966,#3177,.T.);
#6043=EDGE_CURVE('',#4966,#4966,#4247,.T.);
#8162=ORIENTED_EDGE('',*,*,#6038,.F.);
#8163=ORIENTED_EDGE('',*,*,#6039,.T.);
#8164=ORIENTED_EDGE('',*,*,#6040,.T.);
#8165=ORIENTED_EDGE('',*,*,#6039,.F.);
#8166=ORIENTED_EDGE('',*,*,#6041,.F.);
#8167=ORIENTED_EDGE('',*,*,#6042,.T.);
#8168=ORIENTED_EDGE('',*,*,#6043,.T.);
#8169=ORIENTED_EDGE('',*,*,#6042,.F.);
#8170=ORIENTED_EDGE('',*,*,#6041,.T.);
#8171=ORIENTED_EDGE('',*,*,#6038,.T.);
#8172=ORIENTED_EDGE('',*,*,#6043,.F.);
#8173=ORIENTED_EDGE('',*,*,#6040,.F.);
#8499=CYLINDRICAL_SURFACE('',#10651,0.225);
#8500=CYLINDRICAL_SURFACE('',#10654,0.800000000000001);
#9001=ADVANCED_FACE('',(#1810),#8499,.F.);
#9002=ADVANCED_FACE('',(#1811),#8500,.T.);
#9003=ADVANCED_FACE('',(#1812,#997),#1290,.T.);
#9004=ADVANCED_FACE('',(#1813,#998),#1291,.F.);
#9107=CLOSED_SHELL('',(#9001,#9002,#9003,#9004));
#10650=AXIS2_PLACEMENT_3D('',#16915,#13320,#13321);
#10651=AXIS2_PLACEMENT_3D('',#16916,#13322,#13323);
#10652=AXIS2_PLACEMENT_3D('',#16918,#13324,#13325);
#10653=AXIS2_PLACEMENT_3D('',#16921,#13327,#13328);
#10654=AXIS2_PLACEMENT_3D('',#16922,#13329,#13330);
#10655=AXIS2_PLACEMENT_3D('',#16924,#13331,#13332);
#10656=AXIS2_PLACEMENT_3D('',#16927,#13334,#13335);
#10657=AXIS2_PLACEMENT_3D('',#16928,#13336,#13337);
#10658=AXIS2_PLACEMENT_3D('',#16929,#13338,#13339);
#13320=DIRECTION('axis',(0.,0.,1.));
#13321=DIRECTION('refdir',(1.,0.,0.));
#13322=DIRECTION('center_axis',(0.,1.,0.));
#13323=DIRECTION('ref_axis',(1.,0.,0.));
#13324=DIRECTION('center_axis',(0.,-1.,0.));
#13325=DIRECTION('ref_axis',(1.,0.,0.));
#13326=DIRECTION('',(0.,-1.,0.));
#13327=DIRECTION('center_axis',(0.,-1.,0.));
#13328=DIRECTION('ref_axis',(1.,0.,0.));
#13329=DIRECTION('center_axis',(0.,1.,0.));
#13330=DIRECTION('ref_axis',(1.,0.,0.));
#13331=DIRECTION('center_axis',(0.,1.,0.));
#13332=DIRECTION('ref_axis',(1.,0.,0.));
#13333=DIRECTION('',(0.,-1.,0.));
#13334=DIRECTION('center_axis',(0.,1.,0.));
#13335=DIRECTION('ref_axis',(1.,0.,0.));
#13336=DIRECTION('center_axis',(0.,1.,0.));
#13337=DIRECTION('ref_axis',(1.,0.,0.));
#13338=DIRECTION('center_axis',(0.,1.,0.));
#13339=DIRECTION('ref_axis',(1.,0.,0.));
#16915=CARTESIAN_POINT('',(0.,0.,0.));
#16916=CARTESIAN_POINT('Origin',(12.,3.8,10.));
#16917=CARTESIAN_POINT('',(11.775,4.,10.));
#16918=CARTESIAN_POINT('Origin',(12.,4.,10.));
#16919=CARTESIAN_POINT('',(11.775,3.8,10.));
#16920=CARTESIAN_POINT('',(11.775,3.8,10.));
#16921=CARTESIAN_POINT('Origin',(12.,3.8,10.));
#16922=CARTESIAN_POINT('Origin',(12.,3.8,10.));
#16923=CARTESIAN_POINT('',(11.2,4.,10.));
#16924=CARTESIAN_POINT('Origin',(12.,4.,10.));
#16925=CARTESIAN_POINT('',(11.2,3.8,10.));
#16926=CARTESIAN_POINT('',(11.2,3.8,10.));
#16927=CARTESIAN_POINT('Origin',(12.,3.8,10.));
#16928=CARTESIAN_POINT('Origin',(12.,4.,10.));
#16929=CARTESIAN_POINT('Origin',(12.,3.8,10.));
#17256=UNCERTAINTY_MEASURE_WITH_UNIT(LENGTH_MEASURE(0.001),#17323,
'DISTANCE_ACCURACY_VALUE',
'Maximum model space distance between geometric entities at asserted c
onnectivities');
#17261=UNCERTAINTY_MEASURE_WITH_UNIT(LENGTH_MEASURE(0.001),#17323,
'DISTANCE_ACCURACY_VALUE',
'Maximum model space distance between geometric entities at asserted c
onnectivities');
#17317=(
GEOMETRIC_REPRESENTATION_CONTEXT(3)
GLOBAL_UNCERTAINTY_ASSIGNED_CONTEXT((#17256))
GLOBAL_UNIT_ASSIGNED_CONTEXT((#17323,#17325,#17326))
REPRESENTATION_CONTEXT('','3D')
);
#17322=(
GEOMETRIC_REPRESENTATION_CONTEXT(3)
GLOBAL_UNCERTAINTY_ASSIGNED_CONTEXT((#17261))
GLOBAL_UNIT_ASSIGNED_CONTEXT((#17323,#17325,#17326))
REPRESENTATION_CONTEXT('','3D')
);
#17323=(
LENGTH_UNIT()
NAMED_UNIT(*)
SI_UNIT(.CENTI.,.METRE.)
);
#17325=(
NAMED_UNIT(*)
PLANE_ANGLE_UNIT()
SI_UNIT($,.RADIAN.)
);
#17326=(
NAMED_UNIT(*)
SI_UNIT($,.STERADIAN.)
SOLID_ANGLE_UNIT()
);
#17382=SHAPE_DEFINITION_REPRESENTATION(#17456,#17613);
#17456=PRODUCT_DEFINITION_SHAPE('',$,#17674);
#17613=SHAPE_REPRESENTATION('',(#10650),#17317);
#17618=PRODUCT_DEFINITION_CONTEXT('part definition',#17800,'design');
#17674=PRODUCT_DEFINITION('Pin keeper (1)','Pin keeper (1)',#17734,#17618);
#17734=PRODUCT_DEFINITION_FORMATION('',$,#17857);
#17800=APPLICATION_CONTEXT(
'Core Data for Automotive Mechanical Design Process');
#17801=PRODUCT_CONTEXT('part definition',#17800,'mechanical');
#17857=PRODUCT('Pin keeper (1)','Pin keeper (1)','Pin keeper (1)',(#17801));
#17925=COLOUR_RGB('Grey',0.48,0.52,0.57);
#17926=FILL_AREA_STYLE_COLOUR('',#17925);
#17927=FILL_AREA_STYLE('',(#17926));
#17928=SURFACE_STYLE_FILL_AREA(#17927);
#17929=SURFACE_SIDE_STYLE('',(#17928));
#17930=SURFACE_STYLE_USAGE(.BOTH.,#17929);
#17931=PRESENTATION_STYLE_ASSIGNMENT((#17930));
ENDSEC;
END-ISO-10303-21;
